ISO-10303-21;
HEADER;
FILE_DESCRIPTION (('STEP AP214'),
    '1' );
FILE_NAME ('angular contact ball bearing_68_iso_ISO 15 ABB - 178 - 20,SI,NC,20_68.step',
    '2026-10-31T03:41:51',
    ( '' ),
    ( '' ),
    'SwSTEP 2.0',
    'SolidWorks 2026',
    '' );
FILE_SCHEMA (( 'AUTOMOTIVE_DESIGN' ));
ENDSEC;

DATA;
#12=CARTESIAN_POINT ( 'NONE',  ( 0.000000000000000000, 0.000000000000000000, 5.000000000000000000 ) ) ;
#22=ORIENTED_EDGE ( 'NONE', *, *, #685, .T. ) ;
#31=FACE_BOUND ( 'NONE', #5073, .T. ) ;
#37=EDGE_CURVE ( 'NONE', #40, #2037, #3752, .T. ) ;
#40=VERTEX_POINT ( 'NONE', #3206 ) ;
#48=DIRECTION ( 'NONE',  ( 1.000000000000000000, 0.000000000000000000, 0.000000000000000000 ) ) ;
#58=EDGE_CURVE ( 'NONE', #2051, #1778, #6057, .T. ) ;
#82=DIRECTION ( 'NONE',  ( 1.000000000000000000, 0.000000000000000000, 0.000000000000000000 ) ) ;
#83=AXIS2_PLACEMENT_3D ( 'NONE', #12393, #1953, #3185 ) ;
#84=TOROIDAL_SURFACE ( 'NONE', #8934, 5.000000000000000000, 0.5999999999999999778 ) ;
#91=AXIS2_PLACEMENT_3D ( 'NONE', #9821, #7739, #5069 ) ;
#98=DIRECTION ( 'NONE',  ( 0.000000000000000000, 0.000000000000000000, -1.000000000000000000 ) ) ;
#99=VERTEX_POINT ( 'NONE', #962 ) ;
#180=EDGE_CURVE ( 'NONE', #10751, #7956, #7783, .T. ) ;
#181=AXIS2_PLACEMENT_3D ( 'NONE', #7000, #4114, #12760 ) ;
#237=CARTESIAN_POINT ( 'NONE',  ( -1.250000000000001110, 7.286648454926751965E-16, 5.899999999999999467 ) ) ;
#284=ORIENTED_EDGE ( 'NONE', *, *, #11327, .F. ) ;
#296=LINE ( 'NONE', #6688, #7102 ) ;
#335=DIRECTION ( 'NONE',  ( 1.000000000000000000, 0.000000000000000000, 0.000000000000000000 ) ) ;
#337=DIRECTION ( 'NONE',  ( 1.000000000000000000, 0.000000000000000000, 0.000000000000000000 ) ) ;
#359=DIRECTION ( 'NONE',  ( 1.000000000000000000, 0.000000000000000000, 0.000000000000000000 ) ) ;
#371=CIRCLE ( 'NONE', #5552, 0.5999999999999998668 ) ;
#409=AXIS2_PLACEMENT_3D ( 'NONE', #13820, #7911, #6613 ) ;
#443=AXIS2_PLACEMENT_3D ( 'NONE', #14732, #958, #12498 ) ;
#455=ADVANCED_FACE ( 'NONE', ( #8054 ), #3901, .T. ) ;
#536=ORIENTED_EDGE ( 'NONE', *, *, #9442, .F. ) ;
#546=VERTEX_POINT ( 'NONE', #8492 ) ;
#610=PRODUCT_DEFINITION_SHAPE ( 'NONE', 'NONE',  #3183 ) ;
#635=VERTEX_POINT ( 'NONE', #6124 ) ;
#654=AXIS2_PLACEMENT_3D ( 'NONE', #3244, #3311, #6925 ) ;
#680=CARTESIAN_POINT ( 'NONE',  ( -0.1713913650100259145, 0.000000000000000000, 0.000000000000000000 ) ) ;
#681=TOROIDAL_SURFACE ( 'NONE', #3151, 4.100000000000000533, 0.1000000000000001582 ) ;
#685=EDGE_CURVE ( 'NONE', #7400, #10516, #10410, .T. ) ;
#694=ADVANCED_FACE ( 'NONE', ( #3381 ), #10531, .T. ) ;
#695=ORIENTED_EDGE ( 'NONE', *, *, #5681, .F. ) ;
#703=ORIENTED_EDGE ( 'NONE', *, *, #3534, .F. ) ;
#734=ORIENTED_EDGE ( 'NONE', *, *, #37, .F. ) ;
#737=ORIENTED_EDGE ( 'NONE', *, *, #993, .F. ) ;
#739=DIRECTION ( 'NONE',  ( 0.000000000000000000, 0.000000000000000000, -1.000000000000000000 ) ) ;
#752=EDGE_CURVE ( 'NONE', #10751, #2037, #9519, .T. ) ;
#772=DIRECTION ( 'NONE',  ( 0.000000000000000000, -1.000000000000000000, 0.000000000000000000 ) ) ;
#792=ORIENTED_EDGE ( 'NONE', *, *, #2442, .T. ) ;
#843=ORIENTED_EDGE ( 'NONE', *, *, #13220, .F. ) ;
#894=ORIENTED_EDGE ( 'NONE', *, *, #14558, .T. ) ;
#903=DIRECTION ( 'NONE',  ( -0.000000000000000000, 0.000000000000000000, 1.000000000000000000 ) ) ;
#911=DIRECTION ( 'NONE',  ( 0.000000000000000000, 0.000000000000000000, -1.000000000000000000 ) ) ;
#941=CARTESIAN_POINT ( 'NONE',  ( -1.149999999999998135, 5.021051876504148371E-16, 4.100000000000000533 ) ) ;
#942=EDGE_CURVE ( 'NONE', #3736, #15013, #2794, .T. ) ;
#947=DIRECTION ( 'NONE',  ( 0.000000000000000000, 0.000000000000000000, -1.000000000000000000 ) ) ;
#958=DIRECTION ( 'NONE',  ( -1.000000000000000000, -0.000000000000000000, -0.000000000000000000 ) ) ;
#962=CARTESIAN_POINT ( 'NONE',  ( -0.4472135954999577612, 5.633375276077824112E-16, 4.599999999999999645 ) ) ;
#969=CARTESIAN_POINT ( 'NONE',  ( -1.250000000000001110, 0.000000000000000000, -5.575000000000000178 ) ) ;
#980=EDGE_CURVE ( 'NONE', #11004, #15169, #15103, .T. ) ;
#982=DIRECTION ( 'NONE',  ( 0.000000000000000000, 0.000000000000000000, -1.000000000000000000 ) ) ;
#993=EDGE_CURVE ( 'NONE', #5463, #635, #14081, .T. ) ;
#1003=FILL_AREA_STYLE ('',( #7855 ) ) ;
#1047=DIRECTION ( 'NONE',  ( 1.000000000000000000, 0.000000000000000000, 0.000000000000000000 ) ) ;
#1049=ORIENTED_EDGE ( 'NONE', *, *, #13787, .F. ) ;
#1051=AXIS2_PLACEMENT_3D ( 'NONE', #4024, #8698, #9937 ) ;
#1089=CARTESIAN_POINT ( 'NONE',  ( 1.249999999999997558, 0.000000000000000000, 0.000000000000000000 ) ) ;
#1094=ORIENTED_EDGE ( 'NONE', *, *, #10759, .F. ) ;
#1095=FACE_BOUND ( 'NONE', #9322, .T. ) ;
#1149=VERTEX_POINT ( 'NONE', #237 ) ;
#1160=ORIENTED_EDGE ( 'NONE', *, *, #7864, .F. ) ;
#1178=TOROIDAL_SURFACE ( 'NONE', #3629, 5.000000000000000000, 0.5999999999999999778 ) ;
#1214=EDGE_CURVE ( 'NONE', #2185, #99, #4050, .T. ) ;
#1256=CYLINDRICAL_SURFACE ( 'NONE', #13602, 4.000000000000000000 ) ;
#1258=DIRECTION ( 'NONE',  ( 0.000000000000000000, 0.000000000000000000, -1.000000000000000000 ) ) ;
#1304=ADVANCED_FACE ( 'NONE', ( #9929 ), #6556, .T. ) ;
#1322=DIRECTION ( 'NONE',  ( -1.000000000000000000, -0.000000000000000000, -0.000000000000000000 ) ) ;
#1366=CARTESIAN_POINT ( 'NONE',  ( -20.63749999999999929, 0.000000000000000000, 0.000000000000000000 ) ) ;
#1376=AXIS2_PLACEMENT_3D ( 'NONE', #7353, #6187, #9640 ) ;
#1378=VERTEX_POINT ( 'NONE', #3404 ) ;
#1457=EDGE_CURVE ( 'NONE', #7167, #13302, #8454, .T. ) ;
#1464=DIRECTION ( 'NONE',  ( 0.000000000000000000, 0.000000000000000000, 1.000000000000000000 ) ) ;
#1465=CARTESIAN_POINT ( 'NONE',  ( -20.63749999999999929, 0.000000000000000000, -4.424999999999999822 ) ) ;
#1476=TOROIDAL_SURFACE ( 'NONE', #10070, 5.899999999999999467, 0.1000000000000010186 ) ;
#1555=CYLINDRICAL_SURFACE ( 'NONE', #6355, 5.575000000000000178 ) ;
#1573=FACE_OUTER_BOUND ( 'NONE', #3157, .T. ) ;
#1605=FACE_OUTER_BOUND ( 'NONE', #6436, .T. ) ;
#1624=ORIENTED_EDGE ( 'NONE', *, *, #9442, .T. ) ;
#1638=CARTESIAN_POINT ( 'NONE',  ( -20.63749999999999574, 0.000000000000000000, 0.000000000000000000 ) ) ;
#1754=CARTESIAN_POINT ( 'NONE',  ( -1.149999999999998135, 0.000000000000000000, 0.000000000000000000 ) ) ;
#1755=CARTESIAN_POINT ( 'NONE',  ( -1.250000000000001110, 0.000000000000000000, 0.000000000000000000 ) ) ;
#1778=VERTEX_POINT ( 'NONE', #12531 ) ;
#1798=ORIENTED_EDGE ( 'NONE', *, *, #5583, .T. ) ;
#1810=CARTESIAN_POINT ( 'NONE',  ( 0.1713913650100259145, 0.000000000000000000, 4.424999999999999822 ) ) ;
#1819=AXIS2_PLACEMENT_3D ( 'NONE', #3638, #8391, #13159 ) ;
#1821=PRODUCT_CONTEXT ( 'NONE', #10769, 'mechanical' ) ;
#1829=AXIS2_PLACEMENT_3D ( 'NONE', #7372, #8421, #13107 ) ;
#1845=AXIS2_PLACEMENT_3D ( 'NONE', #5193, #14783, #8928 ) ;
#1859=ORIENTED_EDGE ( 'NONE', *, *, #3148, .T. ) ;
#1890=FACE_OUTER_BOUND ( 'NONE', #9487, .T. ) ;
#1896=ORIENTED_EDGE ( 'NONE', *, *, #7500, .T. ) ;
#1899=DIRECTION ( 'NONE',  ( 1.000000000000000000, 0.000000000000000000, 0.000000000000000000 ) ) ;
#1914=CIRCLE ( 'NONE', #14938, 0.1000000000000011297 ) ;
#1918=FACE_OUTER_BOUND ( 'NONE', #12715, .T. ) ;
#1920=ORIENTED_EDGE ( 'NONE', *, *, #180, .F. ) ;
#1923=CYLINDRICAL_SURFACE ( 'NONE', #409, 6.000000000000001776 ) ;
#1928=CIRCLE ( 'NONE', #4390, 4.000000000000000000 ) ;
#1953=DIRECTION ( 'NONE',  ( 1.000000000000000000, 0.000000000000000000, 0.000000000000000000 ) ) ;
#1972=DIRECTION ( 'NONE',  ( 1.000000000000000000, 0.000000000000000000, 0.000000000000000000 ) ) ;
#2007=DIRECTION ( 'NONE',  ( 1.000000000000000000, 0.000000000000000000, 0.000000000000000000 ) ) ;
#2037=VERTEX_POINT ( 'NONE', #12116 ) ;
#2051=VERTEX_POINT ( 'NONE', #8820 ) ;
#2105=ORIENTED_EDGE ( 'NONE', *, *, #2898, .T. ) ;
#2141=ORIENTED_EDGE ( 'NONE', *, *, #980, .F. ) ;
#2150=EDGE_CURVE ( 'NONE', #11004, #7400, #13908, .T. ) ;
#2158=VECTOR ( 'NONE', #12105, 1000.000000000000000 ) ;
#2174=ORIENTED_EDGE ( 'NONE', *, *, #58, .F. ) ;
#2185=VERTEX_POINT ( 'NONE', #3361 ) ;
#2197=CARTESIAN_POINT ( 'NONE',  ( -1.149999999999998135, 0.000000000000000000, 0.000000000000000000 ) ) ;
#2200=EDGE_LOOP ( 'NONE', ( #5137, #8175 ) ) ;
#2203=FACE_OUTER_BOUND ( 'NONE', #11246, .T. ) ;
#2209=DIRECTION ( 'NONE',  ( 1.000000000000000000, 0.000000000000000000, 0.000000000000000000 ) ) ;
#2222=CARTESIAN_POINT ( 'NONE',  ( -1.250000000000001110, 0.000000000000000000, 0.000000000000000000 ) ) ;
#2234=VERTEX_POINT ( 'NONE', #4371 ) ;
#2235=PRESENTATION_STYLE_ASSIGNMENT (( #4242 ) ) ;
#2238=EDGE_LOOP ( 'NONE', ( #13285, #3788, #14789, #4277 ) ) ;
#2249=DIRECTION ( 'NONE',  ( 1.000000000000000000, 0.000000000000000000, 0.000000000000000000 ) ) ;
#2259=ORIENTED_EDGE ( 'NONE', *, *, #2150, .F. ) ;
#2283=LINE ( 'NONE', #14343, #4969 ) ;
#2308=EDGE_CURVE ( 'NONE', #15036, #14991, #9612, .T. ) ;
#2340=DIRECTION ( 'NONE',  ( 1.000000000000000000, 0.000000000000000000, 0.000000000000000000 ) ) ;
#2355=FACE_OUTER_BOUND ( 'NONE', #12520, .T. ) ;
#2377=( NAMED_UNIT ( * ) SI_UNIT ( $, .STERADIAN. ) SOLID_ANGLE_UNIT ( ) );
#2379=ORIENTED_EDGE ( 'NONE', *, *, #11552, .T. ) ;
#2404=DIRECTION ( 'NONE',  ( 0.000000000000000000, 1.000000000000000000, -1.224646799147353207E-16 ) ) ;
#2442=EDGE_CURVE ( 'NONE', #11373, #2185, #2283, .T. ) ;
#2454=DIRECTION ( 'NONE',  ( 0.000000000000000000, 0.000000000000000000, -1.000000000000000000 ) ) ;
#2457=CARTESIAN_POINT ( 'NONE',  ( -20.63749999999999574, 6.827405905246494173E-16, 5.575000000000000178 ) ) ;
#2459=ADVANCED_FACE ( 'NONE', ( #5056 ), #13182, .F. ) ;
#2486=ORIENTED_EDGE ( 'NONE', *, *, #180, .T. ) ;
#2528=ORIENTED_EDGE ( 'NONE', *, *, #5262, .F. ) ;
#2545=ORIENTED_EDGE ( 'NONE', *, *, #14478, .F. ) ;
#2550=ORIENTED_EDGE ( 'NONE', *, *, #1457, .T. ) ;
#2579=CARTESIAN_POINT ( 'NONE',  ( 1.150000000000001688, 0.000000000000000000, 0.000000000000000000 ) ) ;
#2622=AXIS2_PLACEMENT_3D ( 'NONE', #1755, #6439, #11119 ) ;
#2685=DIRECTION ( 'NONE',  ( 0.000000000000000000, 0.000000000000000000, -1.000000000000000000 ) ) ;
#2762=CYLINDRICAL_SURFACE ( 'NONE', #13643, 6.000000000000001776 ) ;
#2782=ADVANCED_FACE ( 'NONE', ( #15032 ), #84, .T. ) ;
#2789=CYLINDRICAL_SURFACE ( 'NONE', #1051, 4.424999999999999822 ) ;
#2794=CIRCLE ( 'NONE', #8938, 4.424999999999999822 ) ;
#2805=AXIS2_PLACEMENT_3D ( 'NONE', #5628, #772, #4469 ) ;
#2814=VECTOR ( 'NONE', #3591, 1000.000000000000000 ) ;
#2834=ORIENTED_EDGE ( 'NONE', *, *, #10095, .F. ) ;
#2859=CIRCLE ( 'NONE', #10946, 5.575000000000000178 ) ;
#2897=ADVANCED_FACE ( 'NONE', ( #11779 ), #1256, .F. ) ;
#2898=EDGE_CURVE ( 'NONE', #10516, #15169, #13842, .T. ) ;
#2958=DIRECTION ( 'NONE',  ( 1.000000000000000000, 0.000000000000000000, 0.000000000000000000 ) ) ;
#2994=DIRECTION ( 'NONE',  ( 1.000000000000000000, 0.000000000000000000, 0.000000000000000000 ) ) ;
#3011=ORIENTED_EDGE ( 'NONE', *, *, #980, .T. ) ;
#3049=AXIS2_PLACEMENT_3D ( 'NONE', #6022, #8390, #10709 ) ;
#3064=DIRECTION ( 'NONE',  ( 0.000000000000000000, 0.000000000000000000, -1.000000000000000000 ) ) ;
#3067=CARTESIAN_POINT ( 'NONE',  ( 1.149999999999998135, 5.021051876504148371E-16, 4.100000000000000533 ) ) ;
#3087=CIRCLE ( 'NONE', #14127, 5.899999999999999467 ) ;
#3116=EDGE_CURVE ( 'NONE', #3736, #546, #9425, .T. ) ;
#3135=EDGE_CURVE ( 'NONE', #13302, #7167, #4785, .T. ) ;
#3148=EDGE_CURVE ( 'NONE', #15013, #10097, #6002, .T. ) ;
#3151=AXIS2_PLACEMENT_3D ( 'NONE', #6810, #1899, #5594 ) ;
#3153=CIRCLE ( 'NONE', #11234, 0.1000000000000002554 ) ;
#3157=EDGE_LOOP ( 'NONE', ( #2550, #11441 ) ) ;
#3183=PRODUCT_DEFINITION ( 'UNKNOWN', '', #12605, #6399 ) ;
#3185=DIRECTION ( 'NONE',  ( 0.000000000000000000, 0.000000000000000000, -1.000000000000000000 ) ) ;
#3192=ORIENTED_EDGE ( 'NONE', *, *, #10838, .T. ) ;
#3201=ORIENTED_EDGE ( 'NONE', *, *, #14543, .F. ) ;
#3206=CARTESIAN_POINT ( 'NONE',  ( 1.149999999999998135, 0.000000000000000000, -4.000000000000000000 ) ) ;
#3224=FACE_BOUND ( 'NONE', #14200, .T. ) ;
#3241=ORIENTED_EDGE ( 'NONE', *, *, #8434, .F. ) ;
#3244=CARTESIAN_POINT ( 'NONE',  ( 1.250000000000001110, 0.000000000000000000, 0.000000000000000000 ) ) ;
#3248=EDGE_CURVE ( 'NONE', #546, #10097, #10419, .T. ) ;
#3254=EDGE_LOOP ( 'NONE', ( #9313, #14348, #6943, #14316 ) ) ;
#3266=MANIFOLD_SOLID_BREP ( 'OuterRace', #9908 ) ;
#3279=DIRECTION ( 'NONE',  ( 0.000000000000000000, 0.000000000000000000, -1.000000000000000000 ) ) ;
#3286=ORIENTED_EDGE ( 'NONE', *, *, #11552, .F. ) ;
#3287=VERTEX_POINT ( 'NONE', #9370 ) ;
#3311=DIRECTION ( 'NONE',  ( 1.000000000000000000, 0.000000000000000000, 0.000000000000000000 ) ) ;
#3361=CARTESIAN_POINT ( 'NONE',  ( -0.4472135954999577612, 0.000000000000000000, -4.599999999999999645 ) ) ;
#3381=FACE_OUTER_BOUND ( 'NONE', #8542, .T. ) ;
#3404=CARTESIAN_POINT ( 'NONE',  ( 1.250000000000001110, 7.286648454926751965E-16, 5.899999999999999467 ) ) ;
#3439=EDGE_LOOP ( 'NONE', ( #3694, #1896, #6611, #14311 ) ) ;
#3449=FACE_OUTER_BOUND ( 'NONE', #3794, .T. ) ;
#3471=EDGE_CURVE ( 'NONE', #1149, #1778, #9491, .T. ) ;
#3478=DIRECTION ( 'NONE',  ( 0.000000000000000000, 0.000000000000000000, -1.000000000000000000 ) ) ;
#3484=DIRECTION ( 'NONE',  ( -1.000000000000000000, -0.000000000000000000, -0.000000000000000000 ) ) ;
#3502=DIRECTION ( 'NONE',  ( -1.000000000000000000, 0.000000000000000000, -0.000000000000000000 ) ) ;
#3509=EDGE_CURVE ( 'NONE', #7956, #40, #4372, .T. ) ;
#3518=DIRECTION ( 'NONE',  ( 0.000000000000000000, 0.000000000000000000, -1.000000000000000000 ) ) ;
#3524=EDGE_LOOP ( 'NONE', ( #1049, #5878, #10762, #3898 ) ) ;
#3534=EDGE_CURVE ( 'NONE', #99, #2185, #4605, .T. ) ;
#3537=EDGE_LOOP ( 'NONE', ( #5144, #10079, #8328, #13567 ) ) ;
#3581=DIRECTION ( 'NONE',  ( 0.000000000000000000, 0.000000000000000000, -1.000000000000000000 ) ) ;
#3585=DIRECTION ( 'NONE',  ( 0.000000000000000000, 0.000000000000000000, 1.000000000000000000 ) ) ;
#3591=DIRECTION ( 'NONE',  ( 1.000000000000000000, 0.000000000000000000, 0.000000000000000000 ) ) ;
#3596=CARTESIAN_POINT ( 'NONE',  ( -20.63749999999999929, 4.898587196589412829E-16, 4.000000000000000000 ) ) ;
#3598=DIRECTION ( 'NONE',  ( 0.000000000000000000, 1.000000000000000000, -1.224646799147353207E-16 ) ) ;
#3629=AXIS2_PLACEMENT_3D ( 'NONE', #11842, #1322, #3706 ) ;
#3632=VERTEX_POINT ( 'NONE', #6968 ) ;
#3638=CARTESIAN_POINT ( 'NONE',  ( -0.1713913650100259145, 0.000000000000000000, 0.000000000000000000 ) ) ;
#3650=ADVANCED_FACE ( 'NONE', ( #7124 ), #8126, .F. ) ;
#3665=AXIS2_PLACEMENT_3D ( 'NONE', #11460, #9238, #5562 ) ;
#3666=ORIENTED_EDGE ( 'NONE', *, *, #2442, .F. ) ;
#3694=ORIENTED_EDGE ( 'NONE', *, *, #12813, .F. ) ;
#3703=ORIENTED_EDGE ( 'NONE', *, *, #10759, .T. ) ;
#3706=DIRECTION ( 'NONE',  ( 0.000000000000000000, 0.000000000000000000, 1.000000000000000000 ) ) ;
#3736=VERTEX_POINT ( 'NONE', #1810 ) ;
#3752=CIRCLE ( 'NONE', #4749, 4.000000000000000000 ) ;
#3770=CARTESIAN_POINT ( 'NONE',  ( 1.150000000000000577, 7.225416114969384193E-16, 5.899999999999999467 ) ) ;
#3788=ORIENTED_EDGE ( 'NONE', *, *, #13787, .T. ) ;
#3794=EDGE_LOOP ( 'NONE', ( #9268, #11771, #5483, #14494 ) ) ;
#3805=DIRECTION ( 'NONE',  ( 0.000000000000000000, 0.000000000000000000, -1.000000000000000000 ) ) ;
#3842=DIRECTION ( 'NONE',  ( 1.000000000000000000, 0.000000000000000000, 0.000000000000000000 ) ) ;
#3862=DIRECTION ( 'NONE',  ( 0.000000000000000000, 1.224646799147351975E-16, 1.000000000000000000 ) ) ;
#3881=CARTESIAN_POINT ( 'NONE',  ( 0.1713913650100259145, 0.000000000000000000, 0.000000000000000000 ) ) ;
#3898=ORIENTED_EDGE ( 'NONE', *, *, #7500, .F. ) ;
#3900=APPLICATION_CONTEXT ( 'automotive_design' ) ;
#3901=TOROIDAL_SURFACE ( 'NONE', #8810, 4.100000000000000533, 0.1000000000000001582 ) ;
#3935=VERTEX_POINT ( 'NONE', #9339 ) ;
#4024=CARTESIAN_POINT ( 'NONE',  ( -20.63749999999999929, 0.000000000000000000, 0.000000000000000000 ) ) ;
#4035=EDGE_CURVE ( 'NONE', #7956, #10751, #12821, .T. ) ;
#4050=CIRCLE ( 'NONE', #1845, 4.599999999999999645 ) ;
#4071=ORIENTED_EDGE ( 'NONE', *, *, #13327, .F. ) ;
#4080=ADVANCED_FACE ( 'NONE', ( #10931 ), #2789, .T. ) ;
#4086=ORIENTED_EDGE ( 'NONE', *, *, #13541, .T. ) ;
#4095=MECHANICAL_DESIGN_GEOMETRIC_PRESENTATION_REPRESENTATION('',(#10716),#14895);
#4114=DIRECTION ( 'NONE',  ( 1.000000000000000000, 0.000000000000000000, 0.000000000000000000 ) ) ;
#4135=AXIS2_PLACEMENT_3D ( 'NONE', #13484, #2958, #7646 ) ;
#4136=CARTESIAN_POINT ( 'NONE',  ( -20.63749999999999574, 7.347880794884121708E-16, 6.000000000000001776 ) ) ;
#4139=AXIS2_PLACEMENT_3D ( 'NONE', #1754, #359, #8660 ) ;
#4171=ORIENTED_EDGE ( 'NONE', *, *, #1457, .F. ) ;
#4206=CARTESIAN_POINT ( 'NONE',  ( 1.149999999999998135, 0.000000000000000000, 0.000000000000000000 ) ) ;
#4216=DIRECTION ( 'NONE',  ( 0.000000000000000000, 0.000000000000000000, 1.000000000000000000 ) ) ;
#4218=ORIENTED_EDGE ( 'NONE', *, *, #6938, .F. ) ;
#4242=SURFACE_STYLE_USAGE ( .BOTH. , #12753 ) ;
#4243=TOROIDAL_SURFACE ( 'NONE', #5238, 4.100000000000000533, 0.1000000000000001582 ) ;
#4277=ORIENTED_EDGE ( 'NONE', *, *, #11712, .F. ) ;
#4283=CARTESIAN_POINT ( 'NONE',  ( 1.250000000000001110, 0.000000000000000000, 0.000000000000000000 ) ) ;
#4285=DIRECTION ( 'NONE',  ( 1.000000000000000000, 0.000000000000000000, 0.000000000000000000 ) ) ;
#4290=CARTESIAN_POINT ( 'NONE',  ( -1.150000000000000577, 7.225416114969384193E-16, 5.899999999999999467 ) ) ;
#4317=AXIS2_PLACEMENT_3D ( 'NONE', #3770, #2404, #3862 ) ;
#4331=ADVANCED_FACE ( 'NONE', ( #6866 ), #4243, .T. ) ;
#4341=( GEOMETRIC_REPRESENTATION_CONTEXT ( 3 ) GLOBAL_UNCERTAINTY_ASSIGNED_CONTEXT ( ( #11150 ) ) GLOBAL_UNIT_ASSIGNED_CONTEXT ( ( #15070, #12677, #6848 ) ) REPRESENTATION_CONTEXT ( 'NONE', 'WORKASPACE' ) );
#4371=CARTESIAN_POINT ( 'NONE',  ( 1.250000000000001110, 6.613092715395707467E-16, 5.400000000000000355 ) ) ;
#4372=LINE ( 'NONE', #5678, #10484 ) ;
#4376=DIRECTION ( 'NONE',  ( -1.000000000000000000, -0.000000000000000000, -0.000000000000000000 ) ) ;
#4382=DIRECTION ( 'NONE',  ( 1.000000000000000000, 0.000000000000000000, 0.000000000000000000 ) ) ;
#4390=AXIS2_PLACEMENT_3D ( 'NONE', #14534, #2994, #6530 ) ;
#4435=CARTESIAN_POINT ( 'NONE',  ( -1.150000000000001688, 0.000000000000000000, 0.000000000000000000 ) ) ;
#4450=DIRECTION ( 'NONE',  ( 1.000000000000000000, 0.000000000000000000, 0.000000000000000000 ) ) ;
#4469=DIRECTION ( 'NONE',  ( 0.000000000000000000, 0.000000000000000000, -1.000000000000000000 ) ) ;
#4478=UNCERTAINTY_MEASURE_WITH_UNIT (LENGTH_MEASURE( 1.000000000000000082E-05 ), #4767, 'distance_accuracy_value', 'NONE');
#4506=ADVANCED_FACE ( 'NONE', ( #3449 ), #11588, .F. ) ;
#4594=CARTESIAN_POINT ( 'NONE',  ( -1.150000000000001688, 0.000000000000000000, 0.000000000000000000 ) ) ;
#4605=CIRCLE ( 'NONE', #14902, 4.599999999999999645 ) ;
#4606=EDGE_LOOP ( 'NONE', ( #4218, #8293, #2379, #5675 ) ) ;
#4623=FACE_OUTER_BOUND ( 'NONE', #11601, .T. ) ;
#4627=CIRCLE ( 'NONE', #4135, 4.100000000000000533 ) ;
#4715=ORIENTED_EDGE ( 'NONE', *, *, #9653, .T. ) ;
#4724=ORIENTED_EDGE ( 'NONE', *, *, #942, .F. ) ;
#4743=CARTESIAN_POINT ( 'NONE',  ( -1.150000000000000577, 0.000000000000000000, 0.000000000000000000 ) ) ;
#4749=AXIS2_PLACEMENT_3D ( 'NONE', #4206, #14881, #739 ) ;
#4764=DIRECTION ( 'NONE',  ( 0.000000000000000000, -1.224646799147353207E-16, 1.000000000000000000 ) ) ;
#4767=( LENGTH_UNIT ( ) NAMED_UNIT ( * ) SI_UNIT ( .MILLI., .METRE. ) );
#4785=CIRCLE ( 'NONE', #12617, 4.424999999999999822 ) ;
#4792=CIRCLE ( 'NONE', #13099, 4.424999999999999822 ) ;
#4797=ORIENTED_EDGE ( 'NONE', *, *, #12293, .T. ) ;
#4808=DIRECTION ( 'NONE',  ( 0.000000000000000000, 0.000000000000000000, -1.000000000000000000 ) ) ;
#4842=ORIENTED_EDGE ( 'NONE', *, *, #3509, .F. ) ;
#4853=ORIENTED_EDGE ( 'NONE', *, *, #1214, .F. ) ;
#4876=CIRCLE ( 'NONE', #7321, 0.5999999999999998668 ) ;
#4879=EDGE_CURVE ( 'NONE', #2234, #7890, #5149, .T. ) ;
#4904=CIRCLE ( 'NONE', #10047, 6.000000000000001776 ) ;
#4916=ORIENTED_EDGE ( 'NONE', *, *, #3135, .F. ) ;
#4969=VECTOR ( 'NONE', #337, 1000.000000000000000 ) ;
#4979=AXIS2_PLACEMENT_3D ( 'NONE', #11741, #12965, #2454 ) ;
#4984=EDGE_CURVE ( 'NONE', #1778, #2051, #4904, .T. ) ;
#4995=AXIS2_PLACEMENT_3D ( 'NONE', #8110, #12782, #1258 ) ;
#5003=CARTESIAN_POINT ( 'NONE',  ( 0.4472135954999577612, 0.000000000000000000, 0.000000000000000000 ) ) ;
#5010=CARTESIAN_POINT ( 'NONE',  ( 1.249999999999997558, 5.419062086227038392E-16, 4.424999999999999822 ) ) ;
#5037=STYLED_ITEM('',(#15272),#3266);
#5047=DIRECTION ( 'NONE',  ( 0.000000000000000000, 0.000000000000000000, -1.000000000000000000 ) ) ;
#5056=FACE_OUTER_BOUND ( 'NONE', #8772, .T. ) ;
#5069=DIRECTION ( 'NONE',  ( 0.000000000000000000, 0.000000000000000000, 1.000000000000000000 ) ) ;
#5073=EDGE_LOOP ( 'NONE', ( #6126, #4086 ) ) ;
#5074=DIRECTION ( 'NONE',  ( 0.000000000000000000, -1.000000000000000000, 0.000000000000000000 ) ) ;
#5097=CARTESIAN_POINT ( 'NONE',  ( 1.249999999999997780, 0.000000000000000000, -4.100000000000000533 ) ) ;
#5117=FACE_OUTER_BOUND ( 'NONE', #9066, .T. ) ;
#5119=CIRCLE ( 'NONE', #181, 4.599999999999999645 ) ;
#5137=ORIENTED_EDGE ( 'NONE', *, *, #14543, .T. ) ;
#5144=ORIENTED_EDGE ( 'NONE', *, *, #3148, .F. ) ;
#5149=CIRCLE ( 'NONE', #10777, 5.400000000000000355 ) ;
#5193=CARTESIAN_POINT ( 'NONE',  ( -0.4472135954999577612, 0.000000000000000000, 0.000000000000000000 ) ) ;
#5218=DIRECTION ( 'NONE',  ( 1.000000000000000000, 0.000000000000000000, 0.000000000000000000 ) ) ;
#5238=AXIS2_PLACEMENT_3D ( 'NONE', #10387, #2249, #12693 ) ;
#5261=DIRECTION ( 'NONE',  ( 0.000000000000000000, 0.000000000000000000, -1.000000000000000000 ) ) ;
#5262=EDGE_CURVE ( 'NONE', #5463, #40, #5647, .T. ) ;
#5348=DIRECTION ( 'NONE',  ( 1.000000000000000000, 0.000000000000000000, 0.000000000000000000 ) ) ;
#5349=FACE_OUTER_BOUND ( 'NONE', #6563, .T. ) ;
#5358=AXIS2_PLACEMENT_3D ( 'NONE', #10234, #5636, #14936 ) ;
#5369=CARTESIAN_POINT ( 'NONE',  ( 1.150000000000000577, 0.000000000000000000, 0.000000000000000000 ) ) ;
#5391=VECTOR ( 'NONE', #3842, 1000.000000000000000 ) ;
#5436=DIRECTION ( 'NONE',  ( 0.000000000000000000, 0.000000000000000000, -1.000000000000000000 ) ) ;
#5463=VERTEX_POINT ( 'NONE', #5097 ) ;
#5483=ORIENTED_EDGE ( 'NONE', *, *, #4879, .T. ) ;
#5537=FACE_OUTER_BOUND ( 'NONE', #3524, .T. ) ;
#5550=DIRECTION ( 'NONE',  ( 0.000000000000000000, 0.000000000000000000, -1.000000000000000000 ) ) ;
#5552=AXIS2_PLACEMENT_3D ( 'NONE', #12, #7168, #3478 ) ;
#5562=DIRECTION ( 'NONE',  ( 0.000000000000000000, 0.000000000000000000, -1.000000000000000000 ) ) ;
#5565=DIRECTION ( 'NONE',  ( 0.000000000000000000, 0.000000000000000000, -1.000000000000000000 ) ) ;
#5583=EDGE_CURVE ( 'NONE', #10097, #7890, #296, .T. ) ;
#5594=DIRECTION ( 'NONE',  ( 0.000000000000000000, 0.000000000000000000, -1.000000000000000000 ) ) ;
#5607=DIRECTION ( 'NONE',  ( 1.000000000000000000, 0.000000000000000000, 0.000000000000000000 ) ) ;
#5627=TOROIDAL_SURFACE ( 'NONE', #6845, 5.899999999999999467, 0.1000000000000010186 ) ;
#5628=CARTESIAN_POINT ( 'NONE',  ( 0.000000000000000000, 0.000000000000000000, 5.000000000000000000 ) ) ;
#5636=DIRECTION ( 'NONE',  ( 1.000000000000000000, 0.000000000000000000, 0.000000000000000000 ) ) ;
#5645=DIRECTION ( 'NONE',  ( 0.000000000000000000, 1.224646799147353207E-16, 1.000000000000000000 ) ) ;
#5647=CIRCLE ( 'NONE', #3665, 0.1000000000000002554 ) ;
#5675=ORIENTED_EDGE ( 'NONE', *, *, #3534, .T. ) ;
#5678=CARTESIAN_POINT ( 'NONE',  ( -20.63749999999999929, 0.000000000000000000, -4.000000000000000000 ) ) ;
#5681=EDGE_CURVE ( 'NONE', #546, #2234, #7990, .T. ) ;
#5749=EDGE_LOOP ( 'NONE', ( #7088, #1859, #11391, #13531 ) ) ;
#5780=AXIS2_PLACEMENT_3D ( 'NONE', #1089, #13845, #5565 ) ;
#5786=ADVANCED_FACE ( 'NONE', ( #4623 ), #10597, .T. ) ;
#5825=AXIS2_PLACEMENT_3D ( 'NONE', #7307, #11976, #1464 ) ;
#5832=DIRECTION ( 'NONE',  ( 1.000000000000000000, 0.000000000000000000, 0.000000000000000000 ) ) ;
#5836=DIRECTION ( 'NONE',  ( -1.000000000000000000, -0.000000000000000000, -0.000000000000000000 ) ) ;
#5846=DIRECTION ( 'NONE',  ( 1.000000000000000000, 0.000000000000000000, 0.000000000000000000 ) ) ;
#5859=CARTESIAN_POINT ( 'NONE',  ( 1.250000000000001110, 0.000000000000000000, 0.000000000000000000 ) ) ;
#5861=CIRCLE ( 'NONE', #14452, 4.100000000000000533 ) ;
#5878=ORIENTED_EDGE ( 'NONE', *, *, #4984, .T. ) ;
#5894=EDGE_CURVE ( 'NONE', #7956, #14052, #8592, .T. ) ;
#5964=CARTESIAN_POINT ( 'NONE',  ( -1.250000000000000666, 5.575000000000000178, 0.000000000000000000 ) ) ;
#5971=ORIENTED_EDGE ( 'NONE', *, *, #14214, .F. ) ;
#6002=CIRCLE ( 'NONE', #14597, 0.5999999999999998668 ) ;
#6022=CARTESIAN_POINT ( 'NONE',  ( -1.150000000000000577, 0.000000000000000000, -5.899999999999999467 ) ) ;
#6057=CIRCLE ( 'NONE', #11930, 6.000000000000001776 ) ;
#6058=LINE ( 'NONE', #11740, #2814 ) ;
#6061=ORIENTED_EDGE ( 'NONE', *, *, #4035, .T. ) ;
#6063=DIRECTION ( 'NONE',  ( 0.000000000000000000, 0.000000000000000000, -1.000000000000000000 ) ) ;
#6116=ADVANCED_FACE ( 'NONE', ( #10346 ), #1476, .T. ) ;
#6124=CARTESIAN_POINT ( 'NONE',  ( 1.249999999999997780, 5.021051876504148371E-16, 4.100000000000000533 ) ) ;
#6126=ORIENTED_EDGE ( 'NONE', *, *, #2150, .T. ) ;
#6151=DIRECTION ( 'NONE',  ( 0.000000000000000000, 0.000000000000000000, -1.000000000000000000 ) ) ;
#6187=DIRECTION ( 'NONE',  ( 0.000000000000000000, 0.000000000000000000, 1.000000000000000000 ) ) ;
#6204=LINE ( 'NONE', #4136, #2158 ) ;
#6259=ORIENTED_EDGE ( 'NONE', *, *, #993, .T. ) ;
#6263=CARTESIAN_POINT ( 'NONE',  ( -1.249999999999997558, 0.000000000000000000, -4.599999999999999645 ) ) ;
#6337=EDGE_LOOP ( 'NONE', ( #10001, #22, #15131, #2141 ) ) ;
#6355=AXIS2_PLACEMENT_3D ( 'NONE', #1638, #12076, #14170 ) ;
#6388=PRODUCT ( 'angular contact ball bearing_68_iso_ISO 15 ABB - 178 - 20,SI,NC,20_68', 'angular contact ball bearing_68_iso_ISO 15 ABB - 178 - 20,SI,NC,20_68', '', ( #1821 ) ) ;
#6399=PRODUCT_DEFINITION_CONTEXT ( 'detailed design', #3900, 'design' ) ;
#6403=CARTESIAN_POINT ( 'NONE',  ( -20.63749999999999574, 0.000000000000000000, 0.000000000000000000 ) ) ;
#6414=DIRECTION ( 'NONE',  ( 0.000000000000000000, 0.000000000000000000, -1.000000000000000000 ) ) ;
#6424=AXIS2_PLACEMENT_3D ( 'NONE', #14194, #14035, #13970 ) ;
#6436=EDGE_LOOP ( 'NONE', ( #6061, #7290, #11123, #6605 ) ) ;
#6439=DIRECTION ( 'NONE',  ( 1.000000000000000000, 0.000000000000000000, 0.000000000000000000 ) ) ;
#6493=MECHANICAL_DESIGN_GEOMETRIC_PRESENTATION_REPRESENTATION('',(#5037),#10913);
#6513=DIRECTION ( 'NONE',  ( 1.000000000000000000, 0.000000000000000000, 0.000000000000000000 ) ) ;
#6530=DIRECTION ( 'NONE',  ( 0.000000000000000000, 0.000000000000000000, -1.000000000000000000 ) ) ;
#6538=CIRCLE ( 'NONE', #8742, 0.1000000000000002554 ) ;
#6556=CYLINDRICAL_SURFACE ( 'NONE', #8695, 4.424999999999999822 ) ;
#6563=EDGE_LOOP ( 'NONE', ( #13247, #10532, #2174, #1160 ) ) ;
#6584=ORIENTED_EDGE ( 'NONE', *, *, #9172, .T. ) ;
#6605=ORIENTED_EDGE ( 'NONE', *, *, #5894, .F. ) ;
#6611=ORIENTED_EDGE ( 'NONE', *, *, #14066, .T. ) ;
#6613=DIRECTION ( 'NONE',  ( 0.000000000000000000, 0.000000000000000000, -1.000000000000000000 ) ) ;
#6640=ADVANCED_FACE ( 'NONE', ( #5117 ), #1555, .F. ) ;
#6688=CARTESIAN_POINT ( 'NONE',  ( -20.63749999999999574, 0.000000000000000000, -5.400000000000000355 ) ) ;
#6710=ADVANCED_FACE ( 'NONE', ( #12154 ), #1178, .T. ) ;
#6733=ADVANCED_FACE ( 'NONE', ( #12239 ), #8929, .F. ) ;
#6750=DIRECTION ( 'NONE',  ( 0.000000000000000000, 1.000000000000000000, -1.224646799147353207E-16 ) ) ;
#6751=DIRECTION ( 'NONE',  ( -1.000000000000000000, 0.000000000000000000, -0.000000000000000000 ) ) ;
#6783=CARTESIAN_POINT ( 'NONE',  ( 0.000000000000000000, 6.123233995736766282E-16, -5.000000000000000000 ) ) ;
#6810=CARTESIAN_POINT ( 'NONE',  ( -1.149999999999998135, 0.000000000000000000, 0.000000000000000000 ) ) ;
#6812=CARTESIAN_POINT ( 'NONE',  ( 0.1713913650100259145, 6.016077400811372436E-16, -4.424999999999999822 ) ) ;
#6845=AXIS2_PLACEMENT_3D ( 'NONE', #5369, #1972, #5436 ) ;
#6848=( NAMED_UNIT ( * ) SI_UNIT ( $, .STERADIAN. ) SOLID_ANGLE_UNIT ( ) );
#6866=FACE_OUTER_BOUND ( 'NONE', #9650, .T. ) ;
#6875=CARTESIAN_POINT ( 'NONE',  ( 0.1713913650100259145, 0.000000000000000000, 0.000000000000000000 ) ) ;
#6891=EDGE_CURVE ( 'NONE', #10751, #3287, #3153, .T. ) ;
#6925=DIRECTION ( 'NONE',  ( 0.000000000000000000, 0.000000000000000000, -1.000000000000000000 ) ) ;
#6938=EDGE_CURVE ( 'NONE', #15169, #2185, #4876, .T. ) ;
#6940=PLANE ( 'NONE',  #7509 ) ;
#6943=ORIENTED_EDGE ( 'NONE', *, *, #3509, .T. ) ;
#6967=CARTESIAN_POINT ( 'NONE',  ( 1.149999999999998135, 0.000000000000000000, 0.000000000000000000 ) ) ;
#6968=CARTESIAN_POINT ( 'NONE',  ( 1.250000000000001110, 0.000000000000000000, -5.899999999999999467 ) ) ;
#7000=CARTESIAN_POINT ( 'NONE',  ( -1.249999999999997558, 0.000000000000000000, 0.000000000000000000 ) ) ;
#7012=ORIENTED_EDGE ( 'NONE', *, *, #4879, .F. ) ;
#7063=CARTESIAN_POINT ( 'NONE',  ( -20.63749999999999929, 0.000000000000000000, 0.000000000000000000 ) ) ;
#7083=TOROIDAL_SURFACE ( 'NONE', #443, 5.000000000000000000, 0.5999999999999999778 ) ;
#7088=ORIENTED_EDGE ( 'NONE', *, *, #942, .T. ) ;
#7102=VECTOR ( 'NONE', #11368, 1000.000000000000000 ) ;
#7110=ADVANCED_FACE ( 'NONE', ( #1605 ), #12710, .T. ) ;
#7124=FACE_OUTER_BOUND ( 'NONE', #14960, .T. ) ;
#7167=VERTEX_POINT ( 'NONE', #12431 ) ;
#7168=DIRECTION ( 'NONE',  ( 0.000000000000000000, -1.000000000000000000, 0.000000000000000000 ) ) ;
#7175=CARTESIAN_POINT ( 'NONE',  ( 0.000000000000000000, 0.000000000000000000, 0.000000000000000000 ) ) ;
#7247=AXIS2_PLACEMENT_3D ( 'NONE', #14649, #13323, #9949 ) ;
#7276=CARTESIAN_POINT ( 'NONE',  ( -20.63749999999999574, 0.000000000000000000, 0.000000000000000000 ) ) ;
#7290=ORIENTED_EDGE ( 'NONE', *, *, #6891, .T. ) ;
#7307=CARTESIAN_POINT ( 'NONE',  ( 0.4472135954999577612, 0.000000000000000000, 0.000000000000000000 ) ) ;
#7313=SHAPE_REPRESENTATION ( 'angular contact ball bearing_68_iso_ISO 15 ABB - 178 - 20,SI,NC,20_68', ( #1376 ), #4341 ) ;
#7321=AXIS2_PLACEMENT_3D ( 'NONE', #6783, #11966, #4764 ) ;
#7329=ADVANCED_FACE ( 'NONE', ( #31, #2355 ), #11645, .T. ) ;
#7353=CARTESIAN_POINT ( 'NONE',  ( 0.000000000000000000, 0.000000000000000000, 0.000000000000000000 ) ) ;
#7372=CARTESIAN_POINT ( 'NONE',  ( -1.249999999999997558, 0.000000000000000000, 0.000000000000000000 ) ) ;
#7400=VERTEX_POINT ( 'NONE', #14267 ) ;
#7478=CARTESIAN_POINT ( 'NONE',  ( -20.63749999999999574, 0.000000000000000000, -6.000000000000001776 ) ) ;
#7500=EDGE_CURVE ( 'NONE', #14991, #15036, #9537, .T. ) ;
#7509=AXIS2_PLACEMENT_3D ( 'NONE', #11613, #9168, #947 ) ;
#7576=ADVANCED_FACE ( 'NONE', ( #1890 ), #7083, .T. ) ;
#7606=ADVANCED_FACE ( 'NONE', ( #10036 ), #5627, .T. ) ;
#7624=EDGE_LOOP ( 'NONE', ( #737, #2834 ) ) ;
#7646=DIRECTION ( 'NONE',  ( 0.000000000000000000, 0.000000000000000000, -1.000000000000000000 ) ) ;
#7739=DIRECTION ( 'NONE',  ( -1.000000000000000000, -0.000000000000000000, -0.000000000000000000 ) ) ;
#7742=DIRECTION ( 'NONE',  ( -1.000000000000000000, -0.000000000000000000, -0.000000000000000000 ) ) ;
#7783=CIRCLE ( 'NONE', #9485, 4.000000000000000000 ) ;
#7815=DIRECTION ( 'NONE',  ( 1.000000000000000000, 0.000000000000000000, 0.000000000000000000 ) ) ;
#7855=FILL_AREA_STYLE_COLOUR ( '', #8746 ) ;
#7864=EDGE_CURVE ( 'NONE', #3935, #2051, #14842, .T. ) ;
#7890=VERTEX_POINT ( 'NONE', #14403 ) ;
#7911=DIRECTION ( 'NONE',  ( 1.000000000000000000, 0.000000000000000000, 0.000000000000000000 ) ) ;
#7924=( NAMED_UNIT ( * ) PLANE_ANGLE_UNIT ( ) SI_UNIT ( $, .RADIAN. ) );
#7941=EDGE_LOOP ( 'NONE', ( #13893, #1624, #14371, #12357 ) ) ;
#7956=VERTEX_POINT ( 'NONE', #9709 ) ;
#7973=ADVANCED_FACE ( 'NONE', ( #5349 ), #13354, .T. ) ;
#7990=LINE ( 'NONE', #10072, #12747 ) ;
#8018=EDGE_LOOP ( 'NONE', ( #9621, #3241, #6584, #4916 ) ) ;
#8054=FACE_OUTER_BOUND ( 'NONE', #11674, .T. ) ;
#8079=SURFACE_STYLE_FILL_AREA ( #1003 ) ;
#8110=CARTESIAN_POINT ( 'NONE',  ( -1.149999999999998135, 0.000000000000000000, 0.000000000000000000 ) ) ;
#8126=CYLINDRICAL_SURFACE ( 'NONE', #15162, 5.400000000000000355 ) ;
#8171=CARTESIAN_POINT ( 'NONE',  ( 1.249999999999997558, 0.000000000000000000, 0.000000000000000000 ) ) ;
#8175=ORIENTED_EDGE ( 'NONE', *, *, #9192, .T. ) ;
#8205=DIRECTION ( 'NONE',  ( 1.000000000000000000, 0.000000000000000000, 0.000000000000000000 ) ) ;
#8250=DIRECTION ( 'NONE',  ( 0.000000000000000000, 0.000000000000000000, -1.000000000000000000 ) ) ;
#8293=ORIENTED_EDGE ( 'NONE', *, *, #12074, .T. ) ;
#8328=ORIENTED_EDGE ( 'NONE', *, *, #3116, .T. ) ;
#8390=DIRECTION ( 'NONE',  ( 0.000000000000000000, -1.000000000000000000, 0.000000000000000000 ) ) ;
#8391=DIRECTION ( 'NONE',  ( -1.000000000000000000, -0.000000000000000000, -0.000000000000000000 ) ) ;
#8421=DIRECTION ( 'NONE',  ( 1.000000000000000000, 0.000000000000000000, 0.000000000000000000 ) ) ;
#8425=CARTESIAN_POINT ( 'NONE',  ( -1.149999999999998135, 0.000000000000000000, -4.100000000000000533 ) ) ;
#8434=EDGE_CURVE ( 'NONE', #15013, #3736, #4792, .T. ) ;
#8454=CIRCLE ( 'NONE', #5780, 4.424999999999999822 ) ;
#8461=DIRECTION ( 'NONE',  ( 1.000000000000000000, 0.000000000000000000, 0.000000000000000000 ) ) ;
#8491=DIRECTION ( 'NONE',  ( 1.000000000000000000, 0.000000000000000000, 0.000000000000000000 ) ) ;
#8492=CARTESIAN_POINT ( 'NONE',  ( 0.4472135954999577612, 0.000000000000000000, 5.400000000000000355 ) ) ;
#8501=LINE ( 'NONE', #11188, #10008 ) ;
#8542=EDGE_LOOP ( 'NONE', ( #11023, #4715, #4853, #3666 ) ) ;
#8555=VECTOR ( 'NONE', #5846, 1000.000000000000000 ) ;
#8574=CARTESIAN_POINT ( 'NONE',  ( -20.63749999999999929, 0.000000000000000000, 0.000000000000000000 ) ) ;
#8592=CIRCLE ( 'NONE', #14500, 0.1000000000000002554 ) ;
#8597=ORIENTED_EDGE ( 'NONE', *, *, #5262, .T. ) ;
#8644=DIRECTION ( 'NONE',  ( 0.000000000000000000, 0.000000000000000000, -1.000000000000000000 ) ) ;
#8660=DIRECTION ( 'NONE',  ( 0.000000000000000000, 0.000000000000000000, -1.000000000000000000 ) ) ;
#8695=AXIS2_PLACEMENT_3D ( 'NONE', #14634, #8852, #11240 ) ;
#8698=DIRECTION ( 'NONE',  ( 1.000000000000000000, 0.000000000000000000, 0.000000000000000000 ) ) ;
#8742=AXIS2_PLACEMENT_3D ( 'NONE', #3067, #6750, #13665 ) ;
#8746=COLOUR_RGB ( '',1.000000000000000000, 0.9490196078431372140, 0.9098039215686274384 ) ;
#8760=CIRCLE ( 'NONE', #5825, 5.400000000000000355 ) ;
#8772=EDGE_LOOP ( 'NONE', ( #1920, #9954, #13502, #4842 ) ) ;
#8810=AXIS2_PLACEMENT_3D ( 'NONE', #6967, #11647, #3581 ) ;
#8815=FACE_OUTER_BOUND ( 'NONE', #4606, .T. ) ;
#8820=CARTESIAN_POINT ( 'NONE',  ( -1.150000000000001688, 0.000000000000000000, -6.000000000000001776 ) ) ;
#8851=ORIENTED_EDGE ( 'NONE', *, *, #6938, .T. ) ;
#8852=DIRECTION ( 'NONE',  ( 1.000000000000000000, 0.000000000000000000, 0.000000000000000000 ) ) ;
#8874=DIRECTION ( 'NONE',  ( 0.000000000000000000, 0.000000000000000000, -1.000000000000000000 ) ) ;
#8919=( LENGTH_UNIT ( ) NAMED_UNIT ( * ) SI_UNIT ( .MILLI., .METRE. ) );
#8928=DIRECTION ( 'NONE',  ( 0.000000000000000000, 0.000000000000000000, -1.000000000000000000 ) ) ;
#8929=CYLINDRICAL_SURFACE ( 'NONE', #11720, 5.575000000000000178 ) ;
#8934=AXIS2_PLACEMENT_3D ( 'NONE', #7175, #3484, #14019 ) ;
#8938=AXIS2_PLACEMENT_3D ( 'NONE', #6875, #7742, #4216 ) ;
#8963=DIRECTION ( 'NONE',  ( 1.000000000000000000, 0.000000000000000000, 0.000000000000000000 ) ) ;
#8982=DIRECTION ( 'NONE',  ( 0.000000000000000000, 0.000000000000000000, -1.000000000000000000 ) ) ;
#9023=ADVANCED_FACE ( 'NONE', ( #12826 ), #9760, .T. ) ;
#9066=EDGE_LOOP ( 'NONE', ( #10938, #2259, #3011, #12993 ) ) ;
#9079=CARTESIAN_POINT ( 'NONE',  ( 1.249999999999997558, 0.000000000000000000, 0.000000000000000000 ) ) ;
#9149=DIRECTION ( 'NONE',  ( 0.000000000000000000, -1.224646799147353207E-16, 1.000000000000000000 ) ) ;
#9168=DIRECTION ( 'NONE',  ( 1.000000000000000000, 0.000000000000000000, 0.000000000000000000 ) ) ;
#9172=EDGE_CURVE ( 'NONE', #15013, #7167, #11825, .T. ) ;
#9192=EDGE_CURVE ( 'NONE', #1378, #3632, #10033, .T. ) ;
#9216=DIRECTION ( 'NONE',  ( 1.000000000000000000, 0.000000000000000000, 0.000000000000000000 ) ) ;
#9238=DIRECTION ( 'NONE',  ( 0.000000000000000000, -1.000000000000000000, 0.000000000000000000 ) ) ;
#9268=ORIENTED_EDGE ( 'NONE', *, *, #3248, .F. ) ;
#9295=AXIS2_PLACEMENT_3D ( 'NONE', #5964, #3502, #10426 ) ;
#9313=ORIENTED_EDGE ( 'NONE', *, *, #752, .F. ) ;
#9315=ORIENTED_EDGE ( 'NONE', *, *, #12813, .T. ) ;
#9322=EDGE_LOOP ( 'NONE', ( #843, #7012 ) ) ;
#9339=CARTESIAN_POINT ( 'NONE',  ( -1.250000000000001110, 0.000000000000000000, -5.899999999999999467 ) ) ;
#9370=CARTESIAN_POINT ( 'NONE',  ( -1.249999999999997780, 5.021051876504148371E-16, 4.100000000000000533 ) ) ;
#9425=CIRCLE ( 'NONE', #2805, 0.5999999999999998668 ) ;
#9442=EDGE_CURVE ( 'NONE', #1149, #3935, #11473, .T. ) ;
#9485=AXIS2_PLACEMENT_3D ( 'NONE', #2197, #2340, #8250 ) ;
#9487=EDGE_LOOP ( 'NONE', ( #2105, #8851, #14943, #3286 ) ) ;
#9488=CARTESIAN_POINT ( 'NONE',  ( -1.249999999999997780, 0.000000000000000000, -4.100000000000000533 ) ) ;
#9491=CIRCLE ( 'NONE', #14663, 0.1000000000000011297 ) ;
#9496=CIRCLE ( 'NONE', #654, 5.400000000000000355 ) ;
#9519=LINE ( 'NONE', #3596, #12372 ) ;
#9536=AXIS2_PLACEMENT_3D ( 'NONE', #13322, #13485, #14569 ) ;
#9537=CIRCLE ( 'NONE', #11006, 6.000000000000000888 ) ;
#9612=CIRCLE ( 'NONE', #6424, 6.000000000000000888 ) ;
#9621=ORIENTED_EDGE ( 'NONE', *, *, #10838, .F. ) ;
#9638=DIRECTION ( 'NONE',  ( 0.000000000000000000, -1.000000000000000000, 0.000000000000000000 ) ) ;
#9640=DIRECTION ( 'NONE',  ( 1.000000000000000000, 0.000000000000000000, 0.000000000000000000 ) ) ;
#9650=EDGE_LOOP ( 'NONE', ( #11767, #9654, #8597, #2545 ) ) ;
#9653=EDGE_CURVE ( 'NONE', #12711, #99, #8501, .T. ) ;
#9654=ORIENTED_EDGE ( 'NONE', *, *, #10095, .T. ) ;
#9689=AXIS2_PLACEMENT_3D ( 'NONE', #5003, #11892, #10674 ) ;
#9702=LINE ( 'NONE', #7478, #9958 ) ;
#9709=CARTESIAN_POINT ( 'NONE',  ( -1.149999999999998135, 0.000000000000000000, -4.000000000000000000 ) ) ;
#9760=TOROIDAL_SURFACE ( 'NONE', #5358, 5.899999999999999467, 0.1000000000000010186 ) ;
#9784=CIRCLE ( 'NONE', #9536, 4.100000000000000533 ) ;
#9802=CARTESIAN_POINT ( 'NONE',  ( 1.150000000000000577, 0.000000000000000000, -5.899999999999999467 ) ) ;
#9821=CARTESIAN_POINT ( 'NONE',  ( 0.000000000000000000, 0.000000000000000000, 0.000000000000000000 ) ) ;
#9824=ADVANCED_FACE ( 'NONE', ( #2203 ), #681, .T. ) ;
#9871=CARTESIAN_POINT ( 'NONE',  ( -1.250000000000001110, 0.000000000000000000, 0.000000000000000000 ) ) ;
#9908=CLOSED_SHELL ( 'NONE', ( #7606, #11868, #7973, #6733, #4506, #7576, #7110, #2459, #455, #694, #1304, #6710, #2782, #4080, #5786, #11308, #4331, #2897, #9824, #12071, #10885, #3650, #6640, #6116, #13548, #9023, #12692, #7329 ) ) ;
#9929=FACE_OUTER_BOUND ( 'NONE', #14546, .T. ) ;
#9937=DIRECTION ( 'NONE',  ( 0.000000000000000000, 0.000000000000000000, -1.000000000000000000 ) ) ;
#9949=DIRECTION ( 'NONE',  ( 0.000000000000000000, 0.000000000000000000, -1.000000000000000000 ) ) ;
#9954=ORIENTED_EDGE ( 'NONE', *, *, #752, .T. ) ;
#9958=VECTOR ( 'NONE', #8461, 1000.000000000000000 ) ;
#10001=ORIENTED_EDGE ( 'NONE', *, *, #13541, .F. ) ;
#10006=CIRCLE ( 'NONE', #14924, 5.575000000000000178 ) ;
#10008=VECTOR ( 'NONE', #5218, 1000.000000000000000 ) ;
#10031=DIRECTION ( 'NONE',  ( 1.000000000000000000, 0.000000000000000000, 0.000000000000000000 ) ) ;
#10033=CIRCLE ( 'NONE', #11984, 5.899999999999999467 ) ;
#10036=FACE_OUTER_BOUND ( 'NONE', #12703, .T. ) ;
#10047=AXIS2_PLACEMENT_3D ( 'NONE', #4594, #1047, #3279 ) ;
#10070=AXIS2_PLACEMENT_3D ( 'NONE', #4743, #2209, #98 ) ;
#10072=CARTESIAN_POINT ( 'NONE',  ( -20.63749999999999574, 6.613092715395707467E-16, 5.400000000000000355 ) ) ;
#10079=ORIENTED_EDGE ( 'NONE', *, *, #8434, .T. ) ;
#10095=EDGE_CURVE ( 'NONE', #635, #5463, #9784, .T. ) ;
#10097=VERTEX_POINT ( 'NONE', #14501 ) ;
#10152=( NAMED_UNIT ( * ) SI_UNIT ( $, .STERADIAN. ) SOLID_ANGLE_UNIT ( ) );
#10234=CARTESIAN_POINT ( 'NONE',  ( 1.150000000000000577, 0.000000000000000000, 0.000000000000000000 ) ) ;
#10342=CARTESIAN_POINT ( 'NONE',  ( 1.150000000000001688, 7.347880794884120722E-16, 6.000000000000000888 ) ) ;
#10346=FACE_OUTER_BOUND ( 'NONE', #7941, .T. ) ;
#10387=CARTESIAN_POINT ( 'NONE',  ( 1.149999999999998135, 0.000000000000000000, 0.000000000000000000 ) ) ;
#10410=LINE ( 'NONE', #2457, #8555 ) ;
#10419=CIRCLE ( 'NONE', #9689, 5.400000000000000355 ) ;
#10426=DIRECTION ( 'NONE',  ( -0.000000000000000000, 0.000000000000000000, 1.000000000000000000 ) ) ;
#10484=VECTOR ( 'NONE', #5607, 1000.000000000000000 ) ;
#10516=VERTEX_POINT ( 'NONE', #14765 ) ;
#10531=CYLINDRICAL_SURFACE ( 'NONE', #15204, 4.599999999999999645 ) ;
#10532=ORIENTED_EDGE ( 'NONE', *, *, #3471, .T. ) ;
#10597=CYLINDRICAL_SURFACE ( 'NONE', #12265, 4.599999999999999645 ) ;
#10632=CARTESIAN_POINT ( 'NONE',  ( -20.63749999999999929, 0.000000000000000000, 0.000000000000000000 ) ) ;
#10674=DIRECTION ( 'NONE',  ( 0.000000000000000000, 0.000000000000000000, 1.000000000000000000 ) ) ;
#10709=DIRECTION ( 'NONE',  ( 0.000000000000000000, 0.000000000000000000, -1.000000000000000000 ) ) ;
#10716=STYLED_ITEM ( 'NONE', ( #2235 ), #13135 ) ;
#10751=VERTEX_POINT ( 'NONE', #12809 ) ;
#10759=EDGE_CURVE ( 'NONE', #12711, #11373, #12379, .T. ) ;
#10762=ORIENTED_EDGE ( 'NONE', *, *, #11712, .T. ) ;
#10769=APPLICATION_CONTEXT ( 'automotive_design' ) ;
#10777=AXIS2_PLACEMENT_3D ( 'NONE', #4283, #8963, #13654 ) ;
#10838=EDGE_CURVE ( 'NONE', #3736, #13302, #6058, .T. ) ;
#10880=ORIENTED_EDGE ( 'NONE', *, *, #9653, .F. ) ;
#10885=ADVANCED_FACE ( 'NONE', ( #8815 ), #15099, .T. ) ;
#10913=( GEOMETRIC_REPRESENTATION_CONTEXT ( 3 ) GLOBAL_UNCERTAINTY_ASSIGNED_CONTEXT ( ( #4478 ) ) GLOBAL_UNIT_ASSIGNED_CONTEXT ( ( #4767, #14134, #2377 ) ) REPRESENTATION_CONTEXT ( 'NONE', 'WORKASPACE' ) );
#10926=CIRCLE ( 'NONE', #4317, 0.1000000000000011297 ) ;
#10931=FACE_OUTER_BOUND ( 'NONE', #8018, .T. ) ;
#10938=ORIENTED_EDGE ( 'NONE', *, *, #685, .F. ) ;
#10943=FACE_BOUND ( 'NONE', #7624, .T. ) ;
#10946=AXIS2_PLACEMENT_3D ( 'NONE', #680, #4376, #982 ) ;
#11004=VERTEX_POINT ( 'NONE', #969 ) ;
#11006=AXIS2_PLACEMENT_3D ( 'NONE', #2579, #335, #3805 ) ;
#11023=ORIENTED_EDGE ( 'NONE', *, *, #14214, .T. ) ;
#11044=SHAPE_DEFINITION_REPRESENTATION ( #610, #7313 ) ;
#11119=DIRECTION ( 'NONE',  ( 0.000000000000000000, 0.000000000000000000, -1.000000000000000000 ) ) ;
#11123=ORIENTED_EDGE ( 'NONE', *, *, #14249, .F. ) ;
#11138=AXIS2_PLACEMENT_3D ( 'NONE', #8171, #4285, #12843 ) ;
#11150=UNCERTAINTY_MEASURE_WITH_UNIT (LENGTH_MEASURE( 1.000000000000000082E-05 ), #15070, 'distance_accuracy_value', 'NONE');
#11188=CARTESIAN_POINT ( 'NONE',  ( -20.63749999999999929, 5.633375276077824112E-16, 4.599999999999999645 ) ) ;
#11207=CARTESIAN_POINT ( 'NONE',  ( -20.63749999999999574, 0.000000000000000000, 0.000000000000000000 ) ) ;
#11234=AXIS2_PLACEMENT_3D ( 'NONE', #941, #3598, #5645 ) ;
#11240=DIRECTION ( 'NONE',  ( 0.000000000000000000, 0.000000000000000000, -1.000000000000000000 ) ) ;
#11246=EDGE_LOOP ( 'NONE', ( #13443, #2486, #13140, #12647 ) ) ;
#11293=CARTESIAN_POINT ( 'NONE',  ( 1.250000000000001110, 0.000000000000000000, 0.000000000000000000 ) ) ;
#11308=ADVANCED_FACE ( 'NONE', ( #1573, #10943 ), #13174, .T. ) ;
#11327=EDGE_CURVE ( 'NONE', #3935, #1149, #3087, .T. ) ;
#11368=DIRECTION ( 'NONE',  ( 1.000000000000000000, 0.000000000000000000, 0.000000000000000000 ) ) ;
#11373=VERTEX_POINT ( 'NONE', #6263 ) ;
#11391=ORIENTED_EDGE ( 'NONE', *, *, #13327, .T. ) ;
#11431=AXIS2_PLACEMENT_3D ( 'NONE', #15054, #6751, #903 ) ;
#11434=DIRECTION ( 'NONE',  ( 1.000000000000000000, 0.000000000000000000, 0.000000000000000000 ) ) ;
#11441=ORIENTED_EDGE ( 'NONE', *, *, #3135, .T. ) ;
#11460=CARTESIAN_POINT ( 'NONE',  ( 1.149999999999998135, 0.000000000000000000, -4.100000000000000533 ) ) ;
#11473=CIRCLE ( 'NONE', #15181, 5.899999999999999467 ) ;
#11507=PLANE ( 'NONE',  #11431 ) ;
#11544=FACE_OUTER_BOUND ( 'NONE', #2200, .T. ) ;
#11552=EDGE_CURVE ( 'NONE', #10516, #99, #371, .T. ) ;
#11588=CYLINDRICAL_SURFACE ( 'NONE', #4979, 5.400000000000000355 ) ;
#11601=EDGE_LOOP ( 'NONE', ( #10880, #3703, #792, #703 ) ) ;
#11613=CARTESIAN_POINT ( 'NONE',  ( 1.250000000000000666, 5.899999999999999467, 0.000000000000000000 ) ) ;
#11645=PLANE ( 'NONE',  #9295 ) ;
#11647=DIRECTION ( 'NONE',  ( 1.000000000000000000, 0.000000000000000000, 0.000000000000000000 ) ) ;
#11671=SHAPE_REPRESENTATION_RELATIONSHIP ( 'NONE' , 'NONE' ,  #7313, #13135 ) ;
#11674=EDGE_LOOP ( 'NONE', ( #6259, #4797, #734, #2528 ) ) ;
#11712=EDGE_CURVE ( 'NONE', #2051, #15036, #9702, .T. ) ;
#11720=AXIS2_PLACEMENT_3D ( 'NONE', #6403, #5348, #5261 ) ;
#11740=CARTESIAN_POINT ( 'NONE',  ( -20.63749999999999929, 5.419062086227038392E-16, 4.424999999999999822 ) ) ;
#11741=CARTESIAN_POINT ( 'NONE',  ( -20.63749999999999574, 0.000000000000000000, 0.000000000000000000 ) ) ;
#11767=ORIENTED_EDGE ( 'NONE', *, *, #12293, .F. ) ;
#11771=ORIENTED_EDGE ( 'NONE', *, *, #5681, .T. ) ;
#11779=FACE_OUTER_BOUND ( 'NONE', #3254, .T. ) ;
#11811=DIRECTION ( 'NONE',  ( 1.000000000000000000, 0.000000000000000000, 0.000000000000000000 ) ) ;
#11825=LINE ( 'NONE', #1465, #5391 ) ;
#11827=AXIS2_PLACEMENT_3D ( 'NONE', #8574, #8491, #8644 ) ;
#11842=CARTESIAN_POINT ( 'NONE',  ( 0.000000000000000000, 0.000000000000000000, 0.000000000000000000 ) ) ;
#11868=ADVANCED_FACE ( 'NONE', ( #13357 ), #2762, .T. ) ;
#11892=DIRECTION ( 'NONE',  ( 1.000000000000000000, 0.000000000000000000, 0.000000000000000000 ) ) ;
#11930=AXIS2_PLACEMENT_3D ( 'NONE', #4435, #7815, #8874 ) ;
#11966=DIRECTION ( 'NONE',  ( -0.000000000000000000, 1.000000000000000000, 1.224646799147353207E-16 ) ) ;
#11976=DIRECTION ( 'NONE',  ( 1.000000000000000000, 0.000000000000000000, 0.000000000000000000 ) ) ;
#11977=DIRECTION ( 'NONE',  ( 1.000000000000000000, 0.000000000000000000, 0.000000000000000000 ) ) ;
#11984=AXIS2_PLACEMENT_3D ( 'NONE', #5859, #11977, #6151 ) ;
#12071=ADVANCED_FACE ( 'NONE', ( #3224, #1918 ), #11507, .T. ) ;
#12074=EDGE_CURVE ( 'NONE', #15169, #10516, #2859, .T. ) ;
#12076=DIRECTION ( 'NONE',  ( 1.000000000000000000, 0.000000000000000000, 0.000000000000000000 ) ) ;
#12105=DIRECTION ( 'NONE',  ( 1.000000000000000000, 0.000000000000000000, 0.000000000000000000 ) ) ;
#12116=CARTESIAN_POINT ( 'NONE',  ( 1.149999999999998135, 4.959819536546779614E-16, 4.000000000000000000 ) ) ;
#12154=FACE_OUTER_BOUND ( 'NONE', #5749, .T. ) ;
#12210=DIRECTION ( 'NONE',  ( 0.000000000000000000, 0.000000000000000000, -1.000000000000000000 ) ) ;
#12239=FACE_OUTER_BOUND ( 'NONE', #6337, .T. ) ;
#12265=AXIS2_PLACEMENT_3D ( 'NONE', #7063, #48, #3518 ) ;
#12293=EDGE_CURVE ( 'NONE', #635, #2037, #6538, .T. ) ;
#12357=ORIENTED_EDGE ( 'NONE', *, *, #4984, .F. ) ;
#12372=VECTOR ( 'NONE', #8205, 1000.000000000000000 ) ;
#12379=CIRCLE ( 'NONE', #1829, 4.599999999999999645 ) ;
#12393=CARTESIAN_POINT ( 'NONE',  ( -1.150000000000000577, 0.000000000000000000, 0.000000000000000000 ) ) ;
#12429=CARTESIAN_POINT ( 'NONE',  ( -20.63749999999999574, 0.000000000000000000, -5.575000000000000178 ) ) ;
#12431=CARTESIAN_POINT ( 'NONE',  ( 1.249999999999997558, 0.000000000000000000, -4.424999999999999822 ) ) ;
#12459=ORIENTED_EDGE ( 'NONE', *, *, #14066, .F. ) ;
#12498=DIRECTION ( 'NONE',  ( 0.000000000000000000, 0.000000000000000000, 1.000000000000000000 ) ) ;
#12520=EDGE_LOOP ( 'NONE', ( #284, #536 ) ) ;
#12531=CARTESIAN_POINT ( 'NONE',  ( -1.150000000000001688, 7.347880794884120722E-16, 6.000000000000001776 ) ) ;
#12605=PRODUCT_DEFINITION_FORMATION_WITH_SPECIFIED_SOURCE ( 'ANY', '', #6388, .NOT_KNOWN. ) ;
#12617=AXIS2_PLACEMENT_3D ( 'NONE', #9079, #2007, #5550 ) ;
#12647=ORIENTED_EDGE ( 'NONE', *, *, #14558, .F. ) ;
#12658=CARTESIAN_POINT ( 'NONE',  ( -1.250000000000001110, 0.000000000000000000, 0.000000000000000000 ) ) ;
#12677=( NAMED_UNIT ( * ) PLANE_ANGLE_UNIT ( ) SI_UNIT ( $, .RADIAN. ) );
#12692=ADVANCED_FACE ( 'NONE', ( #11544, #1095 ), #6940, .T. ) ;
#12693=DIRECTION ( 'NONE',  ( 0.000000000000000000, 0.000000000000000000, -1.000000000000000000 ) ) ;
#12703=EDGE_LOOP ( 'NONE', ( #14914, #9315, #3201, #12459 ) ) ;
#12710=TOROIDAL_SURFACE ( 'NONE', #4139, 4.100000000000000533, 0.1000000000000001582 ) ;
#12711=VERTEX_POINT ( 'NONE', #14007 ) ;
#12715=EDGE_LOOP ( 'NONE', ( #5971, #1094 ) ) ;
#12718=CARTESIAN_POINT ( 'NONE',  ( 1.150000000000001688, 0.000000000000000000, -6.000000000000000888 ) ) ;
#12747=VECTOR ( 'NONE', #13597, 1000.000000000000000 ) ;
#12753=SURFACE_SIDE_STYLE ('',( #8079 ) ) ;
#12760=DIRECTION ( 'NONE',  ( 0.000000000000000000, 0.000000000000000000, -1.000000000000000000 ) ) ;
#12782=DIRECTION ( 'NONE',  ( 1.000000000000000000, 0.000000000000000000, 0.000000000000000000 ) ) ;
#12809=CARTESIAN_POINT ( 'NONE',  ( -1.149999999999998135, 4.898587196589412829E-16, 4.000000000000000000 ) ) ;
#12813=EDGE_CURVE ( 'NONE', #14991, #1378, #10926, .T. ) ;
#12821=CIRCLE ( 'NONE', #4995, 4.000000000000000000 ) ;
#12826=FACE_OUTER_BOUND ( 'NONE', #3439, .T. ) ;
#12843=DIRECTION ( 'NONE',  ( 0.000000000000000000, 0.000000000000000000, -1.000000000000000000 ) ) ;
#12965=DIRECTION ( 'NONE',  ( 1.000000000000000000, 0.000000000000000000, 0.000000000000000000 ) ) ;
#12993=ORIENTED_EDGE ( 'NONE', *, *, #2898, .F. ) ;
#13099=AXIS2_PLACEMENT_3D ( 'NONE', #3881, #5836, #3585 ) ;
#13101=ORIENTED_EDGE ( 'NONE', *, *, #14249, .T. ) ;
#13107=DIRECTION ( 'NONE',  ( 0.000000000000000000, 0.000000000000000000, -1.000000000000000000 ) ) ;
#13135=ADVANCED_BREP_SHAPE_REPRESENTATION ( '', ( #3266, #1376 ), #4341 ) ;
#13140=ORIENTED_EDGE ( 'NONE', *, *, #5894, .T. ) ;
#13159=DIRECTION ( 'NONE',  ( 0.000000000000000000, 0.000000000000000000, -1.000000000000000000 ) ) ;
#13174=PLANE ( 'NONE',  #7247 ) ;
#13182=CYLINDRICAL_SURFACE ( 'NONE', #11827, 4.000000000000000000 ) ;
#13207=CIRCLE ( 'NONE', #15188, 5.899999999999999467 ) ;
#13220=EDGE_CURVE ( 'NONE', #7890, #2234, #9496, .T. ) ;
#13247=ORIENTED_EDGE ( 'NONE', *, *, #11327, .T. ) ;
#13285=ORIENTED_EDGE ( 'NONE', *, *, #58, .T. ) ;
#13302=VERTEX_POINT ( 'NONE', #5010 ) ;
#13322=CARTESIAN_POINT ( 'NONE',  ( 1.249999999999997558, 0.000000000000000000, 0.000000000000000000 ) ) ;
#13323=DIRECTION ( 'NONE',  ( 1.000000000000000000, 0.000000000000000000, 0.000000000000000000 ) ) ;
#13327=EDGE_CURVE ( 'NONE', #10097, #546, #8760, .T. ) ;
#13344=VECTOR ( 'NONE', #6513, 1000.000000000000000 ) ;
#13354=TOROIDAL_SURFACE ( 'NONE', #83, 5.899999999999999467, 0.1000000000000010186 ) ;
#13357=FACE_OUTER_BOUND ( 'NONE', #2238, .T. ) ;
#13440=DIRECTION ( 'NONE',  ( 1.000000000000000000, 0.000000000000000000, 0.000000000000000000 ) ) ;
#13443=ORIENTED_EDGE ( 'NONE', *, *, #6891, .F. ) ;
#13484=CARTESIAN_POINT ( 'NONE',  ( -1.249999999999997558, 0.000000000000000000, 0.000000000000000000 ) ) ;
#13485=DIRECTION ( 'NONE',  ( 1.000000000000000000, 0.000000000000000000, 0.000000000000000000 ) ) ;
#13501=ORIENTED_EDGE ( 'NONE', *, *, #13220, .T. ) ;
#13502=ORIENTED_EDGE ( 'NONE', *, *, #14478, .T. ) ;
#13531=ORIENTED_EDGE ( 'NONE', *, *, #3116, .F. ) ;
#13541=EDGE_CURVE ( 'NONE', #7400, #11004, #10006, .T. ) ;
#13548=ADVANCED_FACE ( 'NONE', ( #5537 ), #1923, .T. ) ;
#13567=ORIENTED_EDGE ( 'NONE', *, *, #3248, .T. ) ;
#13583=DIRECTION ( 'NONE',  ( 0.000000000000000000, 1.000000000000000000, -1.224646799147353207E-16 ) ) ;
#13597=DIRECTION ( 'NONE',  ( 1.000000000000000000, 0.000000000000000000, 0.000000000000000000 ) ) ;
#13602=AXIS2_PLACEMENT_3D ( 'NONE', #10632, #82, #4808 ) ;
#13643=AXIS2_PLACEMENT_3D ( 'NONE', #11207, #13440, #12210 ) ;
#13654=DIRECTION ( 'NONE',  ( 0.000000000000000000, 0.000000000000000000, -1.000000000000000000 ) ) ;
#13665=DIRECTION ( 'NONE',  ( 0.000000000000000000, 1.224646799147353207E-16, 1.000000000000000000 ) ) ;
#13672=DIRECTION ( 'NONE',  ( 0.000000000000000000, 0.000000000000000000, -1.000000000000000000 ) ) ;
#13744=DIRECTION ( 'NONE',  ( 0.000000000000000000, 1.224646799147351975E-16, 1.000000000000000000 ) ) ;
#13787=EDGE_CURVE ( 'NONE', #1778, #14991, #6204, .T. ) ;
#13820=CARTESIAN_POINT ( 'NONE',  ( -20.63749999999999574, 0.000000000000000000, 0.000000000000000000 ) ) ;
#13842=CIRCLE ( 'NONE', #1819, 5.575000000000000178 ) ;
#13845=DIRECTION ( 'NONE',  ( 1.000000000000000000, 0.000000000000000000, 0.000000000000000000 ) ) ;
#13893=ORIENTED_EDGE ( 'NONE', *, *, #3471, .F. ) ;
#13908=CIRCLE ( 'NONE', #2622, 5.575000000000000178 ) ;
#13970=DIRECTION ( 'NONE',  ( 0.000000000000000000, 0.000000000000000000, -1.000000000000000000 ) ) ;
#14007=CARTESIAN_POINT ( 'NONE',  ( -1.249999999999997558, 5.633375276077824112E-16, 4.599999999999999645 ) ) ;
#14019=DIRECTION ( 'NONE',  ( 0.000000000000000000, 0.000000000000000000, 1.000000000000000000 ) ) ;
#14035=DIRECTION ( 'NONE',  ( 1.000000000000000000, 0.000000000000000000, 0.000000000000000000 ) ) ;
#14037=DIRECTION ( 'NONE',  ( 0.000000000000000000, 0.000000000000000000, -1.000000000000000000 ) ) ;
#14052=VERTEX_POINT ( 'NONE', #9488 ) ;
#14066=EDGE_CURVE ( 'NONE', #15036, #3632, #1914, .T. ) ;
#14081=CIRCLE ( 'NONE', #11138, 4.100000000000000533 ) ;
#14127=AXIS2_PLACEMENT_3D ( 'NONE', #9871, #10031, #6414 ) ;
#14134=( NAMED_UNIT ( * ) PLANE_ANGLE_UNIT ( ) SI_UNIT ( $, .RADIAN. ) );
#14170=DIRECTION ( 'NONE',  ( 0.000000000000000000, 0.000000000000000000, -1.000000000000000000 ) ) ;
#14194=CARTESIAN_POINT ( 'NONE',  ( 1.150000000000001688, 0.000000000000000000, 0.000000000000000000 ) ) ;
#14200=EDGE_LOOP ( 'NONE', ( #13101, #894 ) ) ;
#14214=EDGE_CURVE ( 'NONE', #11373, #12711, #5119, .T. ) ;
#14249=EDGE_CURVE ( 'NONE', #14052, #3287, #4627, .T. ) ;
#14267=CARTESIAN_POINT ( 'NONE',  ( -1.250000000000001110, 6.827405905246494173E-16, 5.575000000000000178 ) ) ;
#14311=ORIENTED_EDGE ( 'NONE', *, *, #9192, .F. ) ;
#14316=ORIENTED_EDGE ( 'NONE', *, *, #37, .T. ) ;
#14343=CARTESIAN_POINT ( 'NONE',  ( -20.63749999999999929, 0.000000000000000000, -4.599999999999999645 ) ) ;
#14348=ORIENTED_EDGE ( 'NONE', *, *, #4035, .F. ) ;
#14371=ORIENTED_EDGE ( 'NONE', *, *, #7864, .T. ) ;
#14403=CARTESIAN_POINT ( 'NONE',  ( 1.250000000000001110, 0.000000000000000000, -5.400000000000000355 ) ) ;
#14452=AXIS2_PLACEMENT_3D ( 'NONE', #15142, #9216, #14915 ) ;
#14478=EDGE_CURVE ( 'NONE', #2037, #40, #1928, .T. ) ;
#14494=ORIENTED_EDGE ( 'NONE', *, *, #5583, .F. ) ;
#14500=AXIS2_PLACEMENT_3D ( 'NONE', #8425, #5074, #2685 ) ;
#14501=CARTESIAN_POINT ( 'NONE',  ( 0.4472135954999577612, 6.613092715395707467E-16, -5.400000000000000355 ) ) ;
#14534=CARTESIAN_POINT ( 'NONE',  ( 1.149999999999998135, 0.000000000000000000, 0.000000000000000000 ) ) ;
#14543=EDGE_CURVE ( 'NONE', #3632, #1378, #13207, .T. ) ;
#14546=EDGE_LOOP ( 'NONE', ( #4724, #3192, #4171, #15140 ) ) ;
#14558=EDGE_CURVE ( 'NONE', #3287, #14052, #5861, .T. ) ;
#14569=DIRECTION ( 'NONE',  ( 0.000000000000000000, 0.000000000000000000, -1.000000000000000000 ) ) ;
#14597=AXIS2_PLACEMENT_3D ( 'NONE', #14845, #15067, #9149 ) ;
#14634=CARTESIAN_POINT ( 'NONE',  ( -20.63749999999999929, 0.000000000000000000, 0.000000000000000000 ) ) ;
#14649=CARTESIAN_POINT ( 'NONE',  ( 1.249999999999998002, 4.100000000000000533, 0.000000000000000000 ) ) ;
#14663=AXIS2_PLACEMENT_3D ( 'NONE', #4290, #13583, #13744 ) ;
#14713=UNCERTAINTY_MEASURE_WITH_UNIT (LENGTH_MEASURE( 1.000000000000000082E-05 ), #8919, 'distance_accuracy_value', 'NONE');
#14732=CARTESIAN_POINT ( 'NONE',  ( 0.000000000000000000, 0.000000000000000000, 0.000000000000000000 ) ) ;
#14765=CARTESIAN_POINT ( 'NONE',  ( -0.1713913650100259145, 0.000000000000000000, 5.575000000000000178 ) ) ;
#14783=DIRECTION ( 'NONE',  ( 1.000000000000000000, 0.000000000000000000, 0.000000000000000000 ) ) ;
#14789=ORIENTED_EDGE ( 'NONE', *, *, #2308, .F. ) ;
#14825=CARTESIAN_POINT ( 'NONE',  ( -0.4472135954999577612, 0.000000000000000000, 0.000000000000000000 ) ) ;
#14842=CIRCLE ( 'NONE', #3049, 0.1000000000000011297 ) ;
#14845=CARTESIAN_POINT ( 'NONE',  ( 0.000000000000000000, 6.123233995736766282E-16, -5.000000000000000000 ) ) ;
#14881=DIRECTION ( 'NONE',  ( 1.000000000000000000, 0.000000000000000000, 0.000000000000000000 ) ) ;
#14895=( GEOMETRIC_REPRESENTATION_CONTEXT ( 3 ) GLOBAL_UNCERTAINTY_ASSIGNED_CONTEXT ( ( #14713 ) ) GLOBAL_UNIT_ASSIGNED_CONTEXT ( ( #8919, #7924, #10152 ) ) REPRESENTATION_CONTEXT ( 'NONE', 'WORKASPACE' ) );
#14902=AXIS2_PLACEMENT_3D ( 'NONE', #14825, #4450, #3064 ) ;
#14914=ORIENTED_EDGE ( 'NONE', *, *, #2308, .T. ) ;
#14915=DIRECTION ( 'NONE',  ( 0.000000000000000000, 0.000000000000000000, -1.000000000000000000 ) ) ;
#14924=AXIS2_PLACEMENT_3D ( 'NONE', #12658, #14992, #13672 ) ;
#14936=DIRECTION ( 'NONE',  ( 0.000000000000000000, 0.000000000000000000, -1.000000000000000000 ) ) ;
#14938=AXIS2_PLACEMENT_3D ( 'NONE', #9802, #9638, #5047 ) ;
#14943=ORIENTED_EDGE ( 'NONE', *, *, #1214, .T. ) ;
#14960=EDGE_LOOP ( 'NONE', ( #695, #4071, #1798, #13501 ) ) ;
#14991=VERTEX_POINT ( 'NONE', #10342 ) ;
#14992=DIRECTION ( 'NONE',  ( 1.000000000000000000, 0.000000000000000000, 0.000000000000000000 ) ) ;
#15013=VERTEX_POINT ( 'NONE', #6812 ) ;
#15032=FACE_OUTER_BOUND ( 'NONE', #3537, .T. ) ;
#15036=VERTEX_POINT ( 'NONE', #12718 ) ;
#15054=CARTESIAN_POINT ( 'NONE',  ( -1.249999999999998002, 4.599999999999999645, 0.000000000000000000 ) ) ;
#15067=DIRECTION ( 'NONE',  ( -0.000000000000000000, 1.000000000000000000, 1.224646799147353207E-16 ) ) ;
#15070=( LENGTH_UNIT ( ) NAMED_UNIT ( * ) SI_UNIT ( .MILLI., .METRE. ) );
#15099=TOROIDAL_SURFACE ( 'NONE', #91, 5.000000000000000000, 0.5999999999999999778 ) ;
#15103=LINE ( 'NONE', #12429, #13344 ) ;
#15120=CARTESIAN_POINT ( 'NONE',  ( -0.1713913650100259145, 6.827405905246493187E-16, -5.575000000000000178 ) ) ;
#15131=ORIENTED_EDGE ( 'NONE', *, *, #12074, .F. ) ;
#15140=ORIENTED_EDGE ( 'NONE', *, *, #9172, .F. ) ;
#15142=CARTESIAN_POINT ( 'NONE',  ( -1.249999999999997558, 0.000000000000000000, 0.000000000000000000 ) ) ;
#15162=AXIS2_PLACEMENT_3D ( 'NONE', #7276, #5832, #14037 ) ;
#15169=VERTEX_POINT ( 'NONE', #15120 ) ;
#15181=AXIS2_PLACEMENT_3D ( 'NONE', #2222, #4382, #8982 ) ;
#15188=AXIS2_PLACEMENT_3D ( 'NONE', #11293, #11434, #911 ) ;
#15204=AXIS2_PLACEMENT_3D ( 'NONE', #1366, #11811, #6063 ) ;
#15266=COLOUR_RGB('Grey',0.48,0.52,0.57);
#15267=FILL_AREA_STYLE_COLOUR('',#15266);
#15268=FILL_AREA_STYLE('',(#15267));
#15269=SURFACE_STYLE_FILL_AREA(#15268);
#15270=SURFACE_SIDE_STYLE('',(#15269));
#15271=SURFACE_STYLE_USAGE(.BOTH.,#15270);
#15272=PRESENTATION_STYLE_ASSIGNMENT((#15271));
ENDSEC;
END-ISO-10303-21;
